ISO-10303-21;
HEADER;
/* Generated by software containing ST-Developer
 * from STEP Tools, Inc. (www.steptools.com) 
 */

FILE_DESCRIPTION(
/* description */ ('Four-bar parallelogram arm'),
/* implementation_level */ '2;1');

FILE_NAME(
/* name */ 'Bearing cap (6).step',
/* time_stamp */ '2026-10-28T03:24:55-07:00',
/* author */ (''),
/* organization */ (''),
/* preprocessor_version */ 'ST-DEVELOPER v20.2',
/* originating_system */ 'Autodesk Translation Framework v15.17.0.0',
/* authorisation */ '');

FILE_SCHEMA (('AUTOMOTIVE_DESIGN { 1 0 10303 214 3 1 1 }'));
ENDSEC;

DATA;
#10=MECHANICAL_DESIGN_GEOMETRIC_PRESENTATION_REPRESENTATION('',(#652),#14512);
#552=SHAPE_REPRESENTATION_RELATIONSHIP('SRR','None',#14775,#602);
#602=ADVANCED_BREP_SHAPE_REPRESENTATION('',(#709),#14490);
#652=STYLED_ITEM('',(#15087),#709);
#709=MANIFOLD_SOLID_BREP('Body1',#7357);
#917=FACE_BOUND('',#2053,.T.);
#918=FACE_BOUND('',#2054,.T.);
#919=FACE_BOUND('',#2055,.T.);
#920=FACE_BOUND('',#2056,.T.);
#921=FACE_BOUND('',#2057,.T.);
#922=FACE_BOUND('',#2059,.T.);
#923=FACE_BOUND('',#2060,.T.);
#924=FACE_BOUND('',#2061,.T.);
#925=FACE_BOUND('',#2062,.T.);
#926=FACE_BOUND('',#2063,.T.);
#1123=PLANE('',#8483);
#1124=PLANE('',#8484);
#1444=FACE_OUTER_BOUND('',#2046,.T.);
#1445=FACE_OUTER_BOUND('',#2047,.T.);
#1446=FACE_OUTER_BOUND('',#2048,.T.);
#1447=FACE_OUTER_BOUND('',#2049,.T.);
#1448=FACE_OUTER_BOUND('',#2050,.T.);
#1449=FACE_OUTER_BOUND('',#2051,.T.);
#1450=FACE_OUTER_BOUND('',#2052,.T.);
#1451=FACE_OUTER_BOUND('',#2058,.T.);
#2046=EDGE_LOOP('',(#6012,#6013,#6014,#6015));
#2047=EDGE_LOOP('',(#6016,#6017,#6018,#6019));
#2048=EDGE_LOOP('',(#6020,#6021,#6022,#6023));
#2049=EDGE_LOOP('',(#6024,#6025,#6026,#6027));
#2050=EDGE_LOOP('',(#6028,#6029,#6030,#6031));
#2051=EDGE_LOOP('',(#6032,#6033,#6034,#6035));
#2052=EDGE_LOOP('',(#6036));
#2053=EDGE_LOOP('',(#6037));
#2054=EDGE_LOOP('',(#6038));
#2055=EDGE_LOOP('',(#6039));
#2056=EDGE_LOOP('',(#6040));
#2057=EDGE_LOOP('',(#6041));
#2058=EDGE_LOOP('',(#6042));
#2059=EDGE_LOOP('',(#6043));
#2060=EDGE_LOOP('',(#6044));
#2061=EDGE_LOOP('',(#6045));
#2062=EDGE_LOOP('',(#6046));
#2063=EDGE_LOOP('',(#6047));
#2568=LINE('',#13163,#2962);
#2569=LINE('',#13169,#2963);
#2570=LINE('',#13175,#2964);
#2571=LINE('',#13181,#2965);
#2572=LINE('',#13187,#2966);
#2573=LINE('',#13193,#2967);
#2962=VECTOR('',#10284,0.225000000000001);
#2963=VECTOR('',#10291,0.225000000000001);
#2964=VECTOR('',#10298,0.225000000000001);
#2965=VECTOR('',#10305,0.225000000000001);
#2966=VECTOR('',#10312,1.02);
#2967=VECTOR('',#10319,2.2);
#3350=CIRCLE('',#8466,0.225000000000001);
#3351=CIRCLE('',#8467,0.225000000000001);
#3352=CIRCLE('',#8469,0.225000000000001);
#3353=CIRCLE('',#8470,0.225000000000001);
#3354=CIRCLE('',#8472,0.225000000000001);
#3355=CIRCLE('',#8473,0.225000000000001);
#3356=CIRCLE('',#8475,0.225000000000001);
#3357=CIRCLE('',#8476,0.225000000000001);
#3358=CIRCLE('',#8478,1.02);
#3359=CIRCLE('',#8479,1.02);
#3360=CIRCLE('',#8481,2.2);
#3361=CIRCLE('',#8482,2.2);
#3884=VERTEX_POINT('',#13160);
#3885=VERTEX_POINT('',#13162);
#3886=VERTEX_POINT('',#13166);
#3887=VERTEX_POINT('',#13168);
#3888=VERTEX_POINT('',#13172);
#3889=VERTEX_POINT('',#13174);
#3890=VERTEX_POINT('',#13178);
#3891=VERTEX_POINT('',#13180);
#3892=VERTEX_POINT('',#13184);
#3893=VERTEX_POINT('',#13186);
#3894=VERTEX_POINT('',#13190);
#3895=VERTEX_POINT('',#13192);
#4637=EDGE_CURVE('',#3884,#3884,#3350,.T.);
#4638=EDGE_CURVE('',#3884,#3885,#2568,.T.);
#4639=EDGE_CURVE('',#3885,#3885,#3351,.T.);
#4640=EDGE_CURVE('',#3886,#3886,#3352,.T.);
#4641=EDGE_CURVE('',#3886,#3887,#2569,.T.);
#4642=EDGE_CURVE('',#3887,#3887,#3353,.T.);
#4643=EDGE_CURVE('',#3888,#3888,#3354,.T.);
#4644=EDGE_CURVE('',#3888,#3889,#2570,.T.);
#4645=EDGE_CURVE('',#3889,#3889,#3355,.T.);
#4646=EDGE_CURVE('',#3890,#3890,#3356,.T.);
#4647=EDGE_CURVE('',#3890,#3891,#2571,.T.);
#4648=EDGE_CURVE('',#3891,#3891,#3357,.T.);
#4649=EDGE_CURVE('',#3892,#3892,#3358,.T.);
#4650=EDGE_CURVE('',#3892,#3893,#2572,.T.);
#4651=EDGE_CURVE('',#3893,#3893,#3359,.T.);
#4652=EDGE_CURVE('',#3894,#3894,#3360,.T.);
#4653=EDGE_CURVE('',#3894,#3895,#2573,.T.);
#4654=EDGE_CURVE('',#3895,#3895,#3361,.T.);
#6012=ORIENTED_EDGE('',*,*,#4637,.F.);
#6013=ORIENTED_EDGE('',*,*,#4638,.T.);
#6014=ORIENTED_EDGE('',*,*,#4639,.F.);
#6015=ORIENTED_EDGE('',*,*,#4638,.F.);
#6016=ORIENTED_EDGE('',*,*,#4640,.F.);
#6017=ORIENTED_EDGE('',*,*,#4641,.T.);
#6018=ORIENTED_EDGE('',*,*,#4642,.F.);
#6019=ORIENTED_EDGE('',*,*,#4641,.F.);
#6020=ORIENTED_EDGE('',*,*,#4643,.F.);
#6021=ORIENTED_EDGE('',*,*,#4644,.T.);
#6022=ORIENTED_EDGE('',*,*,#4645,.F.);
#6023=ORIENTED_EDGE('',*,*,#4644,.F.);
#6024=ORIENTED_EDGE('',*,*,#4646,.F.);
#6025=ORIENTED_EDGE('',*,*,#4647,.T.);
#6026=ORIENTED_EDGE('',*,*,#4648,.F.);
#6027=ORIENTED_EDGE('',*,*,#4647,.F.);
#6028=ORIENTED_EDGE('',*,*,#4649,.F.);
#6029=ORIENTED_EDGE('',*,*,#4650,.T.);
#6030=ORIENTED_EDGE('',*,*,#4651,.T.);
#6031=ORIENTED_EDGE('',*,*,#4650,.F.);
#6032=ORIENTED_EDGE('',*,*,#4652,.F.);
#6033=ORIENTED_EDGE('',*,*,#4653,.T.);
#6034=ORIENTED_EDGE('',*,*,#4654,.T.);
#6035=ORIENTED_EDGE('',*,*,#4653,.F.);
#6036=ORIENTED_EDGE('',*,*,#4652,.T.);
#6037=ORIENTED_EDGE('',*,*,#4649,.T.);
#6038=ORIENTED_EDGE('',*,*,#4648,.T.);
#6039=ORIENTED_EDGE('',*,*,#4645,.T.);
#6040=ORIENTED_EDGE('',*,*,#4642,.T.);
#6041=ORIENTED_EDGE('',*,*,#4639,.T.);
#6042=ORIENTED_EDGE('',*,*,#4654,.F.);
#6043=ORIENTED_EDGE('',*,*,#4651,.F.);
#6044=ORIENTED_EDGE('',*,*,#4646,.T.);
#6045=ORIENTED_EDGE('',*,*,#4643,.T.);
#6046=ORIENTED_EDGE('',*,*,#4640,.T.);
#6047=ORIENTED_EDGE('',*,*,#4637,.T.);
#6836=CYLINDRICAL_SURFACE('',#8465,0.225000000000001);
#6837=CYLINDRICAL_SURFACE('',#8468,0.225000000000001);
#6838=CYLINDRICAL_SURFACE('',#8471,0.225000000000001);
#6839=CYLINDRICAL_SURFACE('',#8474,0.225000000000001);
#6840=CYLINDRICAL_SURFACE('',#8477,1.02);
#6841=CYLINDRICAL_SURFACE('',#8480,2.2);
#7149=ADVANCED_FACE('',(#1444),#6836,.F.);
#7150=ADVANCED_FACE('',(#1445),#6837,.F.);
#7151=ADVANCED_FACE('',(#1446),#6838,.F.);
#7152=ADVANCED_FACE('',(#1447),#6839,.F.);
#7153=ADVANCED_FACE('',(#1448),#6840,.F.);
#7154=ADVANCED_FACE('',(#1449),#6841,.T.);
#7155=ADVANCED_FACE('',(#1450,#917,#918,#919,#920,#921),#1123,.T.);
#7156=ADVANCED_FACE('',(#1451,#922,#923,#924,#925,#926),#1124,.F.);
#7357=CLOSED_SHELL('',(#7149,#7150,#7151,#7152,#7153,#7154,#7155,#7156));
#8464=AXIS2_PLACEMENT_3D('',#13158,#10278,#10279);
#8465=AXIS2_PLACEMENT_3D('',#13159,#10280,#10281);
#8466=AXIS2_PLACEMENT_3D('',#13161,#10282,#10283);
#8467=AXIS2_PLACEMENT_3D('',#13164,#10285,#10286);
#8468=AXIS2_PLACEMENT_3D('',#13165,#10287,#10288);
#8469=AXIS2_PLACEMENT_3D('',#13167,#10289,#10290);
#8470=AXIS2_PLACEMENT_3D('',#13170,#10292,#10293);
#8471=AXIS2_PLACEMENT_3D('',#13171,#10294,#10295);
#8472=AXIS2_PLACEMENT_3D('',#13173,#10296,#10297);
#8473=AXIS2_PLACEMENT_3D('',#13176,#10299,#10300);
#8474=AXIS2_PLACEMENT_3D('',#13177,#10301,#10302);
#8475=AXIS2_PLACEMENT_3D('',#13179,#10303,#10304);
#8476=AXIS2_PLACEMENT_3D('',#13182,#10306,#10307);
#8477=AXIS2_PLACEMENT_3D('',#13183,#10308,#10309);
#8478=AXIS2_PLACEMENT_3D('',#13185,#10310,#10311);
#8479=AXIS2_PLACEMENT_3D('',#13188,#10313,#10314);
#8480=AXIS2_PLACEMENT_3D('',#13189,#10315,#10316);
#8481=AXIS2_PLACEMENT_3D('',#13191,#10317,#10318);
#8482=AXIS2_PLACEMENT_3D('',#13194,#10320,#10321);
#8483=AXIS2_PLACEMENT_3D('',#13195,#10322,#10323);
#8484=AXIS2_PLACEMENT_3D('',#13196,#10324,#10325);
#10278=DIRECTION('axis',(0.,0.,1.));
#10279=DIRECTION('refdir',(1.,0.,0.));
#10280=DIRECTION('center_axis',(0.,1.,0.));
#10281=DIRECTION('ref_axis',(1.,0.,0.));
#10282=DIRECTION('center_axis',(0.,1.,0.));
#10283=DIRECTION('ref_axis',(1.,0.,0.));
#10284=DIRECTION('',(0.,1.,0.));
#10285=DIRECTION('center_axis',(0.,-1.,0.));
#10286=DIRECTION('ref_axis',(1.,0.,0.));
#10287=DIRECTION('center_axis',(0.,1.,0.));
#10288=DIRECTION('ref_axis',(1.,0.,0.));
#10289=DIRECTION('center_axis',(0.,1.,0.));
#10290=DIRECTION('ref_axis',(1.,0.,0.));
#10291=DIRECTION('',(0.,1.,0.));
#10292=DIRECTION('center_axis',(0.,-1.,0.));
#10293=DIRECTION('ref_axis',(1.,0.,0.));
#10294=DIRECTION('center_axis',(0.,1.,0.));
#10295=DIRECTION('ref_axis',(1.,0.,0.));
#10296=DIRECTION('center_axis',(0.,1.,0.));
#10297=DIRECTION('ref_axis',(1.,0.,0.));
#10298=DIRECTION('',(0.,1.,0.));
#10299=DIRECTION('center_axis',(0.,-1.,0.));
#10300=DIRECTION('ref_axis',(1.,0.,0.));
#10301=DIRECTION('center_axis',(0.,1.,0.));
#10302=DIRECTION('ref_axis',(1.,0.,0.));
#10303=DIRECTION('center_axis',(0.,1.,0.));
#10304=DIRECTION('ref_axis',(1.,0.,0.));
#10305=DIRECTION('',(0.,1.,0.));
#10306=DIRECTION('center_axis',(0.,-1.,0.));
#10307=DIRECTION('ref_axis',(1.,0.,0.));
#10308=DIRECTION('center_axis',(0.,1.,0.));
#10309=DIRECTION('ref_axis',(1.,0.,0.));
#10310=DIRECTION('center_axis',(0.,-1.,0.));
#10311=DIRECTION('ref_axis',(1.,0.,0.));
#10312=DIRECTION('',(0.,-1.,0.));
#10313=DIRECTION('center_axis',(0.,-1.,0.));
#10314=DIRECTION('ref_axis',(1.,0.,0.));
#10315=DIRECTION('center_axis',(0.,1.,0.));
#10316=DIRECTION('ref_axis',(1.,0.,0.));
#10317=DIRECTION('center_axis',(0.,1.,0.));
#10318=DIRECTION('ref_axis',(1.,0.,0.));
#10319=DIRECTION('',(0.,-1.,0.));
#10320=DIRECTION('center_axis',(0.,1.,0.));
#10321=DIRECTION('ref_axis',(1.,0.,0.));
#10322=DIRECTION('center_axis',(0.,1.,0.));
#10323=DIRECTION('ref_axis',(1.,0.,0.));
#10324=DIRECTION('center_axis',(0.,1.,0.));
#10325=DIRECTION('ref_axis',(1.,0.,0.));
#13158=CARTESIAN_POINT('',(0.,0.,0.));
#13159=CARTESIAN_POINT('Origin',(18.7625631329235,-1.5,12.7625631329235));
#13160=CARTESIAN_POINT('',(18.5375631329235,-1.4,12.7625631329235));
#13161=CARTESIAN_POINT('Origin',(18.7625631329235,-1.4,12.7625631329235));
#13162=CARTESIAN_POINT('',(18.5375631329235,-1.05,12.7625631329235));
#13163=CARTESIAN_POINT('',(18.5375631329235,-1.5,12.7625631329235));
#13164=CARTESIAN_POINT('Origin',(18.7625631329235,-1.05,12.7625631329235));
#13165=CARTESIAN_POINT('Origin',(18.7625631329235,-1.5,15.2374368670765));
#13166=CARTESIAN_POINT('',(18.5375631329235,-1.4,15.2374368670765));
#13167=CARTESIAN_POINT('Origin',(18.7625631329235,-1.4,15.2374368670765));
#13168=CARTESIAN_POINT('',(18.5375631329235,-1.05,15.2374368670765));
#13169=CARTESIAN_POINT('',(18.5375631329235,-1.5,15.2374368670765));
#13170=CARTESIAN_POINT('Origin',(18.7625631329235,-1.05,15.2374368670765));
#13171=CARTESIAN_POINT('Origin',(21.2374368670765,-1.5,15.2374368670765));
#13172=CARTESIAN_POINT('',(21.0124368670765,-1.4,15.2374368670765));
#13173=CARTESIAN_POINT('Origin',(21.2374368670765,-1.4,15.2374368670765));
#13174=CARTESIAN_POINT('',(21.0124368670765,-1.05,15.2374368670765));
#13175=CARTESIAN_POINT('',(21.0124368670765,-1.5,15.2374368670765));
#13176=CARTESIAN_POINT('Origin',(21.2374368670765,-1.05,15.2374368670765));
#13177=CARTESIAN_POINT('Origin',(21.2374368670765,-1.5,12.7625631329235));
#13178=CARTESIAN_POINT('',(21.0124368670765,-1.4,12.7625631329235));
#13179=CARTESIAN_POINT('Origin',(21.2374368670765,-1.4,12.7625631329235));
#13180=CARTESIAN_POINT('',(21.0124368670765,-1.05,12.7625631329235));
#13181=CARTESIAN_POINT('',(21.0124368670765,-1.5,12.7625631329235));
#13182=CARTESIAN_POINT('Origin',(21.2374368670765,-1.05,12.7625631329235));
#13183=CARTESIAN_POINT('Origin',(20.,-1.4,14.));
#13184=CARTESIAN_POINT('',(18.98,-1.05,14.));
#13185=CARTESIAN_POINT('Origin',(20.,-1.05,14.));
#13186=CARTESIAN_POINT('',(18.98,-1.4,14.));
#13187=CARTESIAN_POINT('',(18.98,-1.4,14.));
#13188=CARTESIAN_POINT('Origin',(20.,-1.4,14.));
#13189=CARTESIAN_POINT('Origin',(20.,-1.4,14.));
#13190=CARTESIAN_POINT('',(17.8,-1.05,14.));
#13191=CARTESIAN_POINT('Origin',(20.,-1.05,14.));
#13192=CARTESIAN_POINT('',(17.8,-1.4,14.));
#13193=CARTESIAN_POINT('',(17.8,-1.4,14.));
#13194=CARTESIAN_POINT('Origin',(20.,-1.4,14.));
#13195=CARTESIAN_POINT('Origin',(20.,-1.05,14.));
#13196=CARTESIAN_POINT('Origin',(20.,-1.4,14.));
#14433=UNCERTAINTY_MEASURE_WITH_UNIT(LENGTH_MEASURE(0.001),#14513,
'DISTANCE_ACCURACY_VALUE',
'Maximum model space distance between geometric entities at asserted c
onnectivities');
#14455=UNCERTAINTY_MEASURE_WITH_UNIT(LENGTH_MEASURE(0.001),#14513,
'DISTANCE_ACCURACY_VALUE',
'Maximum model space distance between geometric entities at asserted c
onnectivities');
#14490=(
GEOMETRIC_REPRESENTATION_CONTEXT(3)
GLOBAL_UNCERTAINTY_ASSIGNED_CONTEXT((#14433))
GLOBAL_UNIT_ASSIGNED_CONTEXT((#14513,#14515,#14516))
REPRESENTATION_CONTEXT('','3D')
);
#14512=(
GEOMETRIC_REPRESENTATION_CONTEXT(3)
GLOBAL_UNCERTAINTY_ASSIGNED_CONTEXT((#14455))
GLOBAL_UNIT_ASSIGNED_CONTEXT((#14513,#14515,#14516))
REPRESENTATION_CONTEXT('','3D')
);
#14513=(
LENGTH_UNIT()
NAMED_UNIT(*)
SI_UNIT(.CENTI.,.METRE.)
);
#14515=(
NAMED_UNIT(*)
PLANE_ANGLE_UNIT()
SI_UNIT($,.RADIAN.)
);
#14516=(
NAMED_UNIT(*)
SI_UNIT($,.STERADIAN.)
SOLID_ANGLE_UNIT()
);
#14551=SHAPE_DEFINITION_REPRESENTATION(#14607,#14775);
#14607=PRODUCT_DEFINITION_SHAPE('',$,#14832);
#14775=SHAPE_REPRESENTATION('',(#8464),#14490);
#14797=PRODUCT_DEFINITION_CONTEXT('part definition',#14967,'design');
#14832=PRODUCT_DEFINITION('Bearing cap (6)','Bearing cap (6)',#14888,#14797);
#14888=PRODUCT_DEFINITION_FORMATION('',$,#15003);
#14967=APPLICATION_CONTEXT(
'Core Data for Automotive Mechanical Design Process');
#14968=PRODUCT_CONTEXT('part definition',#14967,'mechanical');
#15003=PRODUCT('Bearing cap (6)','Bearing cap (6)','Bearing cap (6)',(#14968));
#15081=COLOUR_RGB('Grey',0.48,0.52,0.57);
#15082=FILL_AREA_STYLE_COLOUR('',#15081);
#15083=FILL_AREA_STYLE('',(#15082));
#15084=SURFACE_STYLE_FILL_AREA(#15083);
#15085=SURFACE_SIDE_STYLE('',(#15084));
#15086=SURFACE_STYLE_USAGE(.BOTH.,#15085);
#15087=PRESENTATION_STYLE_ASSIGNMENT((#15086));
ENDSEC;
END-ISO-10303-21;
